ISO-10303-21;
HEADER;
/* Generated by software containing ST-Developer
 * from STEP Tools, Inc. (www.steptools.com) 
 */

FILE_DESCRIPTION(
/* description */ ('PAT-080'),
/* implementation_level */ '2;1');

FILE_NAME(
/* name */ 'Pipe Elbow - 90 Degrees, 1-2 Inch Tapered Pipe Thread.step',
/* time_stamp */ '2026-10-29T20:13:47-07:00',
/* author */ (''),
/* organization */ (''),
/* preprocessor_version */ 'ST-DEVELOPER v20.2',
/* originating_system */ 'Autodesk Translation Framework v15.17.0.0',
/* authorisation */ '');

FILE_SCHEMA (('AUTOMOTIVE_DESIGN { 1 0 10303 214 3 1 1 }'));
ENDSEC;

DATA;
#10=MECHANICAL_DESIGN_GEOMETRIC_PRESENTATION_REPRESENTATION('',(#260),#6878);
#183=SPHERICAL_SURFACE('',#4385,0.837);
#184=SPHERICAL_SURFACE('',#4399,1.2);
#185=ELLIPSE('',#4381,1.11722871427475,0.79);
#186=ELLIPSE('',#4405,1.69705627484771,1.2);
#222=SHAPE_REPRESENTATION_RELATIONSHIP('SRR','None',#6978,#241);
#241=ADVANCED_BREP_SHAPE_REPRESENTATION('',(#277),#6873);
#260=STYLED_ITEM('',(#7115),#277);
#277=MANIFOLD_SOLID_BREP('Body1',#3878);
#341=FACE_BOUND('',#951,.T.);
#342=FACE_BOUND('',#954,.T.);
#343=FACE_BOUND('',#958,.T.);
#344=FACE_BOUND('',#962,.T.);
#345=FACE_BOUND('',#965,.T.);
#346=FACE_BOUND('',#967,.T.);
#347=FACE_BOUND('',#970,.T.);
#463=PLANE('',#4391);
#464=PLANE('',#4398);
#465=PLANE('',#4407);
#466=PLANE('',#4411);
#467=PLANE('',#4412);
#468=PLANE('',#4417);
#663=FACE_OUTER_BOUND('',#949,.T.);
#664=FACE_OUTER_BOUND('',#950,.T.);
#665=FACE_OUTER_BOUND('',#952,.T.);
#666=FACE_OUTER_BOUND('',#953,.T.);
#667=FACE_OUTER_BOUND('',#955,.T.);
#668=FACE_OUTER_BOUND('',#956,.T.);
#669=FACE_OUTER_BOUND('',#957,.T.);
#670=FACE_OUTER_BOUND('',#959,.T.);
#671=FACE_OUTER_BOUND('',#960,.T.);
#672=FACE_OUTER_BOUND('',#961,.T.);
#673=FACE_OUTER_BOUND('',#963,.T.);
#674=FACE_OUTER_BOUND('',#964,.T.);
#675=FACE_OUTER_BOUND('',#966,.T.);
#676=FACE_OUTER_BOUND('',#968,.T.);
#677=FACE_OUTER_BOUND('',#969,.T.);
#678=FACE_OUTER_BOUND('',#971,.T.);
#949=EDGE_LOOP('',(#3320,#3321,#3322,#3323,#3324,#3325));
#950=EDGE_LOOP('',(#3326,#3327));
#951=EDGE_LOOP('',(#3328,#3329,#3330,#3331));
#952=EDGE_LOOP('',(#3332,#3333,#3334,#3335,#3336,#3337));
#953=EDGE_LOOP('',(#3338));
#954=EDGE_LOOP('',(#3339));
#955=EDGE_LOOP('',(#3340,#3341,#3342,#3343));
#956=EDGE_LOOP('',(#3344,#3345,#3346,#3347));
#957=EDGE_LOOP('',(#3348));
#958=EDGE_LOOP('',(#3349));
#959=EDGE_LOOP('',(#3350,#3351,#3352,#3353));
#960=EDGE_LOOP('',(#3354,#3355,#3356,#3357,#3358,#3359));
#961=EDGE_LOOP('',(#3360));
#962=EDGE_LOOP('',(#3361));
#963=EDGE_LOOP('',(#3362,#3363,#3364,#3365));
#964=EDGE_LOOP('',(#3366));
#965=EDGE_LOOP('',(#3367));
#966=EDGE_LOOP('',(#3368));
#967=EDGE_LOOP('',(#3369));
#968=EDGE_LOOP('',(#3370,#3371,#3372,#3373));
#969=EDGE_LOOP('',(#3374));
#970=EDGE_LOOP('',(#3375));
#971=EDGE_LOOP('',(#3376,#3377,#3378,#3379,#3380,#3381));
#1277=LINE('',#6506,#1592);
#1278=LINE('',#6518,#1593);
#1279=LINE('',#6526,#1594);
#1280=LINE('',#6531,#1595);
#1281=LINE('',#6546,#1596);
#1282=LINE('',#6554,#1597);
#1283=LINE('',#6564,#1598);
#1284=LINE('',#6567,#1599);
#1592=VECTOR('',#5361,0.79);
#1593=VECTOR('',#5376,0.79);
#1594=VECTOR('',#5387,0.93);
#1595=VECTOR('',#5392,0.93);
#1596=VECTOR('',#5411,1.2);
#1597=VECTOR('',#5422,1.45);
#1598=VECTOR('',#5435,1.45);
#1599=VECTOR('',#5440,1.2);
#1765=CIRCLE('',#4382,0.79);
#1766=CIRCLE('',#4383,0.79);
#1767=CIRCLE('',#4384,0.79);
#1768=CIRCLE('',#4386,0.837);
#1769=CIRCLE('',#4387,0.79);
#1770=CIRCLE('',#4388,0.79);
#1771=CIRCLE('',#4390,0.79);
#1772=CIRCLE('',#4392,0.93);
#1773=CIRCLE('',#4394,0.93);
#1774=CIRCLE('',#4396,0.93);
#1775=CIRCLE('',#4397,0.93);
#1776=CIRCLE('',#4400,1.2);
#1777=CIRCLE('',#4401,1.2);
#1778=CIRCLE('',#4402,1.2);
#1779=CIRCLE('',#4403,1.2);
#1780=CIRCLE('',#4406,1.2);
#1781=CIRCLE('',#4408,1.45);
#1782=CIRCLE('',#4410,1.45);
#1783=CIRCLE('',#4413,1.45);
#1784=CIRCLE('',#4414,1.2);
#1785=CIRCLE('',#4416,1.45);
#2045=VERTEX_POINT('',#6500);
#2046=VERTEX_POINT('',#6501);
#2047=VERTEX_POINT('',#6503);
#2048=VERTEX_POINT('',#6505);
#2049=VERTEX_POINT('',#6510);
#2050=VERTEX_POINT('',#6511);
#2051=VERTEX_POINT('',#6513);
#2052=VERTEX_POINT('',#6517);
#2053=VERTEX_POINT('',#6521);
#2054=VERTEX_POINT('',#6524);
#2055=VERTEX_POINT('',#6528);
#2056=VERTEX_POINT('',#6530);
#2057=VERTEX_POINT('',#6535);
#2058=VERTEX_POINT('',#6536);
#2059=VERTEX_POINT('',#6538);
#2060=VERTEX_POINT('',#6540);
#2061=VERTEX_POINT('',#6545);
#2062=VERTEX_POINT('',#6549);
#2063=VERTEX_POINT('',#6552);
#2064=VERTEX_POINT('',#6557);
#2065=VERTEX_POINT('',#6559);
#2066=VERTEX_POINT('',#6562);
#2483=EDGE_CURVE('',#2045,#2046,#185,.T.);
#2484=EDGE_CURVE('',#2047,#2045,#1765,.T.);
#2485=EDGE_CURVE('',#2047,#2048,#1277,.T.);
#2486=EDGE_CURVE('',#2048,#2048,#1766,.T.);
#2487=EDGE_CURVE('',#2046,#2047,#1767,.T.);
#2488=EDGE_CURVE('',#2049,#2050,#1768,.T.);
#2489=EDGE_CURVE('',#2045,#2051,#1769,.T.);
#2490=EDGE_CURVE('',#2051,#2046,#1770,.T.);
#2491=EDGE_CURVE('',#2051,#2052,#1278,.T.);
#2492=EDGE_CURVE('',#2052,#2052,#1771,.T.);
#2493=EDGE_CURVE('',#2053,#2053,#1772,.T.);
#2494=EDGE_CURVE('',#2054,#2054,#1773,.T.);
#2495=EDGE_CURVE('',#2054,#2053,#1279,.T.);
#2496=EDGE_CURVE('',#2055,#2055,#1774,.T.);
#2497=EDGE_CURVE('',#2055,#2056,#1280,.T.);
#2498=EDGE_CURVE('',#2056,#2056,#1775,.T.);
#2499=EDGE_CURVE('',#2057,#2058,#1776,.T.);
#2500=EDGE_CURVE('',#2058,#2059,#1777,.T.);
#2501=EDGE_CURVE('',#2060,#2059,#1778,.T.);
#2502=EDGE_CURVE('',#2057,#2060,#1779,.T.);
#2503=EDGE_CURVE('',#2059,#2057,#186,.T.);
#2504=EDGE_CURVE('',#2058,#2061,#1281,.T.);
#2505=EDGE_CURVE('',#2061,#2061,#1780,.T.);
#2506=EDGE_CURVE('',#2062,#2062,#1781,.T.);
#2507=EDGE_CURVE('',#2063,#2063,#1782,.T.);
#2508=EDGE_CURVE('',#2063,#2062,#1282,.T.);
#2509=EDGE_CURVE('',#2064,#2064,#1783,.T.);
#2510=EDGE_CURVE('',#2065,#2065,#1784,.T.);
#2511=EDGE_CURVE('',#2066,#2066,#1785,.T.);
#2512=EDGE_CURVE('',#2066,#2064,#1283,.T.);
#2513=EDGE_CURVE('',#2065,#2060,#1284,.T.);
#3320=ORIENTED_EDGE('',*,*,#2483,.F.);
#3321=ORIENTED_EDGE('',*,*,#2484,.F.);
#3322=ORIENTED_EDGE('',*,*,#2485,.T.);
#3323=ORIENTED_EDGE('',*,*,#2486,.F.);
#3324=ORIENTED_EDGE('',*,*,#2485,.F.);
#3325=ORIENTED_EDGE('',*,*,#2487,.F.);
#3326=ORIENTED_EDGE('',*,*,#2488,.T.);
#3327=ORIENTED_EDGE('',*,*,#2488,.F.);
#3328=ORIENTED_EDGE('',*,*,#2487,.T.);
#3329=ORIENTED_EDGE('',*,*,#2484,.T.);
#3330=ORIENTED_EDGE('',*,*,#2489,.T.);
#3331=ORIENTED_EDGE('',*,*,#2490,.T.);
#3332=ORIENTED_EDGE('',*,*,#2483,.T.);
#3333=ORIENTED_EDGE('',*,*,#2490,.F.);
#3334=ORIENTED_EDGE('',*,*,#2491,.T.);
#3335=ORIENTED_EDGE('',*,*,#2492,.F.);
#3336=ORIENTED_EDGE('',*,*,#2491,.F.);
#3337=ORIENTED_EDGE('',*,*,#2489,.F.);
#3338=ORIENTED_EDGE('',*,*,#2493,.F.);
#3339=ORIENTED_EDGE('',*,*,#2486,.T.);
#3340=ORIENTED_EDGE('',*,*,#2494,.F.);
#3341=ORIENTED_EDGE('',*,*,#2495,.T.);
#3342=ORIENTED_EDGE('',*,*,#2493,.T.);
#3343=ORIENTED_EDGE('',*,*,#2495,.F.);
#3344=ORIENTED_EDGE('',*,*,#2496,.F.);
#3345=ORIENTED_EDGE('',*,*,#2497,.T.);
#3346=ORIENTED_EDGE('',*,*,#2498,.F.);
#3347=ORIENTED_EDGE('',*,*,#2497,.F.);
#3348=ORIENTED_EDGE('',*,*,#2496,.T.);
#3349=ORIENTED_EDGE('',*,*,#2492,.T.);
#3350=ORIENTED_EDGE('',*,*,#2499,.T.);
#3351=ORIENTED_EDGE('',*,*,#2500,.T.);
#3352=ORIENTED_EDGE('',*,*,#2501,.F.);
#3353=ORIENTED_EDGE('',*,*,#2502,.F.);
#3354=ORIENTED_EDGE('',*,*,#2503,.F.);
#3355=ORIENTED_EDGE('',*,*,#2500,.F.);
#3356=ORIENTED_EDGE('',*,*,#2504,.T.);
#3357=ORIENTED_EDGE('',*,*,#2505,.T.);
#3358=ORIENTED_EDGE('',*,*,#2504,.F.);
#3359=ORIENTED_EDGE('',*,*,#2499,.F.);
#3360=ORIENTED_EDGE('',*,*,#2506,.F.);
#3361=ORIENTED_EDGE('',*,*,#2494,.T.);
#3362=ORIENTED_EDGE('',*,*,#2507,.F.);
#3363=ORIENTED_EDGE('',*,*,#2508,.T.);
#3364=ORIENTED_EDGE('',*,*,#2506,.T.);
#3365=ORIENTED_EDGE('',*,*,#2508,.F.);
#3366=ORIENTED_EDGE('',*,*,#2507,.T.);
#3367=ORIENTED_EDGE('',*,*,#2505,.F.);
#3368=ORIENTED_EDGE('',*,*,#2509,.F.);
#3369=ORIENTED_EDGE('',*,*,#2510,.T.);
#3370=ORIENTED_EDGE('',*,*,#2511,.F.);
#3371=ORIENTED_EDGE('',*,*,#2512,.T.);
#3372=ORIENTED_EDGE('',*,*,#2509,.T.);
#3373=ORIENTED_EDGE('',*,*,#2512,.F.);
#3374=ORIENTED_EDGE('',*,*,#2511,.T.);
#3375=ORIENTED_EDGE('',*,*,#2498,.T.);
#3376=ORIENTED_EDGE('',*,*,#2510,.F.);
#3377=ORIENTED_EDGE('',*,*,#2513,.T.);
#3378=ORIENTED_EDGE('',*,*,#2501,.T.);
#3379=ORIENTED_EDGE('',*,*,#2503,.T.);
#3380=ORIENTED_EDGE('',*,*,#2502,.T.);
#3381=ORIENTED_EDGE('',*,*,#2513,.F.);
#3620=CYLINDRICAL_SURFACE('',#4380,0.79);
#3621=CYLINDRICAL_SURFACE('',#4389,0.79);
#3622=CYLINDRICAL_SURFACE('',#4393,0.93);
#3623=CYLINDRICAL_SURFACE('',#4395,0.93);
#3624=CYLINDRICAL_SURFACE('',#4404,1.2);
#3625=CYLINDRICAL_SURFACE('',#4409,1.45);
#3626=CYLINDRICAL_SURFACE('',#4415,1.45);
#3627=CYLINDRICAL_SURFACE('',#4418,1.2);
#3799=ADVANCED_FACE('',(#663),#3620,.F.);
#3800=ADVANCED_FACE('',(#664,#341),#183,.F.);
#3801=ADVANCED_FACE('',(#665),#3621,.F.);
#3802=ADVANCED_FACE('',(#666,#342),#463,.F.);
#3803=ADVANCED_FACE('',(#667),#3622,.F.);
#3804=ADVANCED_FACE('',(#668),#3623,.F.);
#3805=ADVANCED_FACE('',(#669,#343),#464,.F.);
#3806=ADVANCED_FACE('',(#670),#184,.T.);
#3807=ADVANCED_FACE('',(#671),#3624,.T.);
#3808=ADVANCED_FACE('',(#672,#344),#465,.T.);
#3809=ADVANCED_FACE('',(#673),#3625,.T.);
#3810=ADVANCED_FACE('',(#674,#345),#466,.T.);
#3811=ADVANCED_FACE('',(#675,#346),#467,.T.);
#3812=ADVANCED_FACE('',(#676),#3626,.T.);
#3813=ADVANCED_FACE('',(#677,#347),#468,.T.);
#3814=ADVANCED_FACE('',(#678),#3627,.T.);
#3878=CLOSED_SHELL('',(#3799,#3800,#3801,#3802,#3803,#3804,#3805,#3806,
#3807,#3808,#3809,#3810,#3811,#3812,#3813,#3814));
#4379=AXIS2_PLACEMENT_3D('',#6498,#5353,#5354);
#4380=AXIS2_PLACEMENT_3D('',#6499,#5355,#5356);
#4381=AXIS2_PLACEMENT_3D('',#6502,#5357,#5358);
#4382=AXIS2_PLACEMENT_3D('',#6504,#5359,#5360);
#4383=AXIS2_PLACEMENT_3D('',#6507,#5362,#5363);
#4384=AXIS2_PLACEMENT_3D('',#6508,#5364,#5365);
#4385=AXIS2_PLACEMENT_3D('',#6509,#5366,#5367);
#4386=AXIS2_PLACEMENT_3D('',#6512,#5368,#5369);
#4387=AXIS2_PLACEMENT_3D('',#6514,#5370,#5371);
#4388=AXIS2_PLACEMENT_3D('',#6515,#5372,#5373);
#4389=AXIS2_PLACEMENT_3D('',#6516,#5374,#5375);
#4390=AXIS2_PLACEMENT_3D('',#6519,#5377,#5378);
#4391=AXIS2_PLACEMENT_3D('',#6520,#5379,#5380);
#4392=AXIS2_PLACEMENT_3D('',#6522,#5381,#5382);
#4393=AXIS2_PLACEMENT_3D('',#6523,#5383,#5384);
#4394=AXIS2_PLACEMENT_3D('',#6525,#5385,#5386);
#4395=AXIS2_PLACEMENT_3D('',#6527,#5388,#5389);
#4396=AXIS2_PLACEMENT_3D('',#6529,#5390,#5391);
#4397=AXIS2_PLACEMENT_3D('',#6532,#5393,#5394);
#4398=AXIS2_PLACEMENT_3D('',#6533,#5395,#5396);
#4399=AXIS2_PLACEMENT_3D('',#6534,#5397,#5398);
#4400=AXIS2_PLACEMENT_3D('',#6537,#5399,#5400);
#4401=AXIS2_PLACEMENT_3D('',#6539,#5401,#5402);
#4402=AXIS2_PLACEMENT_3D('',#6541,#5403,#5404);
#4403=AXIS2_PLACEMENT_3D('',#6542,#5405,#5406);
#4404=AXIS2_PLACEMENT_3D('',#6543,#5407,#5408);
#4405=AXIS2_PLACEMENT_3D('',#6544,#5409,#5410);
#4406=AXIS2_PLACEMENT_3D('',#6547,#5412,#5413);
#4407=AXIS2_PLACEMENT_3D('',#6548,#5414,#5415);
#4408=AXIS2_PLACEMENT_3D('',#6550,#5416,#5417);
#4409=AXIS2_PLACEMENT_3D('',#6551,#5418,#5419);
#4410=AXIS2_PLACEMENT_3D('',#6553,#5420,#5421);
#4411=AXIS2_PLACEMENT_3D('',#6555,#5423,#5424);
#4412=AXIS2_PLACEMENT_3D('',#6556,#5425,#5426);
#4413=AXIS2_PLACEMENT_3D('',#6558,#5427,#5428);
#4414=AXIS2_PLACEMENT_3D('',#6560,#5429,#5430);
#4415=AXIS2_PLACEMENT_3D('',#6561,#5431,#5432);
#4416=AXIS2_PLACEMENT_3D('',#6563,#5433,#5434);
#4417=AXIS2_PLACEMENT_3D('',#6565,#5436,#5437);
#4418=AXIS2_PLACEMENT_3D('',#6566,#5438,#5439);
#5353=DIRECTION('axis',(0.,0.,1.));
#5354=DIRECTION('refdir',(1.,0.,0.));
#5355=DIRECTION('center_axis',(0.,1.,0.));
#5356=DIRECTION('ref_axis',(1.,0.,0.));
#5357=DIRECTION('center_axis',(-0.707106781186548,0.707106781186548,0.));
#5358=DIRECTION('ref_axis',(0.707106781186547,0.707106781186547,0.));
#5359=DIRECTION('center_axis',(0.,1.,0.));
#5360=DIRECTION('ref_axis',(1.,0.,0.));
#5361=DIRECTION('',(0.,1.,0.));
#5362=DIRECTION('center_axis',(0.,-1.,0.));
#5363=DIRECTION('ref_axis',(1.,0.,0.));
#5364=DIRECTION('center_axis',(0.,1.,0.));
#5365=DIRECTION('ref_axis',(1.,0.,0.));
#5366=DIRECTION('center_axis',(6.12323399573677E-17,0.,1.));
#5367=DIRECTION('ref_axis',(1.,0.,0.));
#5368=DIRECTION('center_axis',(-1.22464679914735E-16,1.,0.));
#5369=DIRECTION('ref_axis',(-1.,-1.22464679914735E-16,0.));
#5370=DIRECTION('center_axis',(1.,0.,0.));
#5371=DIRECTION('ref_axis',(0.,0.,-1.));
#5372=DIRECTION('center_axis',(1.,0.,0.));
#5373=DIRECTION('ref_axis',(0.,0.,-1.));
#5374=DIRECTION('center_axis',(1.,0.,0.));
#5375=DIRECTION('ref_axis',(0.,0.,-1.));
#5376=DIRECTION('',(1.,0.,0.));
#5377=DIRECTION('center_axis',(-1.,0.,0.));
#5378=DIRECTION('ref_axis',(0.,0.,-1.));
#5379=DIRECTION('center_axis',(0.,-1.,0.));
#5380=DIRECTION('ref_axis',(0.,0.,-1.));
#5381=DIRECTION('center_axis',(0.,-1.,0.));
#5382=DIRECTION('ref_axis',(1.,0.,0.));
#5383=DIRECTION('center_axis',(0.,-1.,0.));
#5384=DIRECTION('ref_axis',(1.,0.,0.));
#5385=DIRECTION('center_axis',(0.,-1.,0.));
#5386=DIRECTION('ref_axis',(1.,0.,0.));
#5387=DIRECTION('',(0.,-1.,0.));
#5388=DIRECTION('center_axis',(1.,0.,0.));
#5389=DIRECTION('ref_axis',(0.,1.,0.));
#5390=DIRECTION('center_axis',(1.,0.,0.));
#5391=DIRECTION('ref_axis',(0.,0.,-1.));
#5392=DIRECTION('',(1.,0.,0.));
#5393=DIRECTION('center_axis',(-1.,0.,0.));
#5394=DIRECTION('ref_axis',(0.,1.,0.));
#5395=DIRECTION('center_axis',(-1.,0.,0.));
#5396=DIRECTION('ref_axis',(0.,0.,1.));
#5397=DIRECTION('center_axis',(6.12323399573677E-17,0.,1.));
#5398=DIRECTION('ref_axis',(1.,0.,0.));
#5399=DIRECTION('center_axis',(0.,-1.,0.));
#5400=DIRECTION('ref_axis',(1.,0.,0.));
#5401=DIRECTION('center_axis',(0.,-1.,0.));
#5402=DIRECTION('ref_axis',(1.,0.,0.));
#5403=DIRECTION('center_axis',(1.,0.,0.));
#5404=DIRECTION('ref_axis',(0.,0.,-1.));
#5405=DIRECTION('center_axis',(1.,0.,0.));
#5406=DIRECTION('ref_axis',(0.,0.,-1.));
#5407=DIRECTION('center_axis',(0.,-1.,0.));
#5408=DIRECTION('ref_axis',(1.,0.,0.));
#5409=DIRECTION('center_axis',(0.707106781186548,-0.707106781186548,0.));
#5410=DIRECTION('ref_axis',(0.707106781186547,0.707106781186547,0.));
#5411=DIRECTION('',(0.,1.,0.));
#5412=DIRECTION('center_axis',(0.,-1.,0.));
#5413=DIRECTION('ref_axis',(1.,0.,0.));
#5414=DIRECTION('center_axis',(0.,1.,0.));
#5415=DIRECTION('ref_axis',(0.,0.,1.));
#5416=DIRECTION('center_axis',(0.,-1.,0.));
#5417=DIRECTION('ref_axis',(1.,0.,0.));
#5418=DIRECTION('center_axis',(0.,-1.,0.));
#5419=DIRECTION('ref_axis',(1.,0.,0.));
#5420=DIRECTION('center_axis',(0.,-1.,0.));
#5421=DIRECTION('ref_axis',(1.,0.,0.));
#5422=DIRECTION('',(0.,1.,0.));
#5423=DIRECTION('center_axis',(0.,-1.,0.));
#5424=DIRECTION('ref_axis',(0.,0.,-1.));
#5425=DIRECTION('center_axis',(-1.,0.,0.));
#5426=DIRECTION('ref_axis',(0.,0.,1.));
#5427=DIRECTION('center_axis',(1.,0.,0.));
#5428=DIRECTION('ref_axis',(0.,0.,-1.));
#5429=DIRECTION('center_axis',(1.,0.,0.));
#5430=DIRECTION('ref_axis',(0.,0.,-1.));
#5431=DIRECTION('center_axis',(1.,0.,0.));
#5432=DIRECTION('ref_axis',(0.,1.,0.));
#5433=DIRECTION('center_axis',(1.,0.,0.));
#5434=DIRECTION('ref_axis',(0.,0.,-1.));
#5435=DIRECTION('',(-1.,0.,0.));
#5436=DIRECTION('center_axis',(1.,0.,0.));
#5437=DIRECTION('ref_axis',(0.,0.,-1.));
#5438=DIRECTION('center_axis',(1.,0.,0.));
#5439=DIRECTION('ref_axis',(0.,1.,0.));
#5440=DIRECTION('',(-1.,0.,0.));
#6498=CARTESIAN_POINT('',(0.,0.,0.));
#6499=CARTESIAN_POINT('Origin',(0.,0.,0.));
#6500=CARTESIAN_POINT('',(0.276530287672074,0.276530287672074,0.740020945649513));
#6501=CARTESIAN_POINT('',(0.276530287672074,0.276530287672074,-0.740020945649513));
#6502=CARTESIAN_POINT('Origin',(0.,0.,0.));
#6503=CARTESIAN_POINT('',(-0.79,0.276530287672074,9.67470971326409E-17));
#6504=CARTESIAN_POINT('Origin',(0.,0.276530287672074,0.));
#6505=CARTESIAN_POINT('',(-0.79,1.45,-9.67470971326409E-17));
#6506=CARTESIAN_POINT('',(-0.79,0.,9.67470971326409E-17));
#6507=CARTESIAN_POINT('Origin',(0.,1.45,0.));
#6508=CARTESIAN_POINT('Origin',(0.,0.276530287672074,0.));
#6509=CARTESIAN_POINT('Origin',(0.,0.,0.));
#6510=CARTESIAN_POINT('',(-5.12514685443167E-17,-6.27649469043988E-33,-0.837));
#6511=CARTESIAN_POINT('',(-5.12514685443167E-17,-6.27649469043988E-33,0.837));
#6512=CARTESIAN_POINT('Origin',(0.,0.,0.));
#6513=CARTESIAN_POINT('',(0.276530287672074,-9.67470971326409E-17,0.79));
#6514=CARTESIAN_POINT('Origin',(0.276530287672074,0.,0.));
#6515=CARTESIAN_POINT('Origin',(0.276530287672074,0.,0.));
#6516=CARTESIAN_POINT('Origin',(0.,0.,0.));
#6517=CARTESIAN_POINT('',(1.45,9.67470971326409E-17,0.79));
#6518=CARTESIAN_POINT('',(0.,-9.67470971326409E-17,0.79));
#6519=CARTESIAN_POINT('Origin',(1.45,0.,0.));
#6520=CARTESIAN_POINT('Origin',(0.,1.45,0.));
#6521=CARTESIAN_POINT('',(-0.93,1.45,-1.13892152320704E-16));
#6522=CARTESIAN_POINT('Origin',(0.,1.45,0.));
#6523=CARTESIAN_POINT('Origin',(0.,2.175,0.));
#6524=CARTESIAN_POINT('',(-0.93,2.8,-1.13892152320704E-16));
#6525=CARTESIAN_POINT('Origin',(0.,2.8,0.));
#6526=CARTESIAN_POINT('',(-0.93,2.175,-1.13892152320704E-16));
#6527=CARTESIAN_POINT('Origin',(2.175,0.,0.));
#6528=CARTESIAN_POINT('',(1.45,-0.93,-1.13892152320704E-16));
#6529=CARTESIAN_POINT('Origin',(1.45,0.,0.));
#6530=CARTESIAN_POINT('',(2.8,-0.93,1.13892152320704E-16));
#6531=CARTESIAN_POINT('',(2.175,-0.93,-1.13892152320704E-16));
#6532=CARTESIAN_POINT('Origin',(2.8,0.,0.));
#6533=CARTESIAN_POINT('Origin',(1.45,0.93,0.));
#6534=CARTESIAN_POINT('Origin',(0.,0.,0.));
#6535=CARTESIAN_POINT('',(0.,0.,1.2));
#6536=CARTESIAN_POINT('',(-1.2,1.11022302462516E-16,-1.46957615897682E-16));
#6537=CARTESIAN_POINT('Origin',(0.,0.,0.));
#6538=CARTESIAN_POINT('',(0.,0.,-1.2));
#6539=CARTESIAN_POINT('Origin',(0.,0.,0.));
#6540=CARTESIAN_POINT('',(1.11022302462516E-16,-1.2,-1.46957615897682E-16));
#6541=CARTESIAN_POINT('Origin',(0.,0.,0.));
#6542=CARTESIAN_POINT('Origin',(0.,0.,0.));
#6543=CARTESIAN_POINT('Origin',(0.,0.9,0.));
#6544=CARTESIAN_POINT('Origin',(0.,0.,0.));
#6545=CARTESIAN_POINT('',(-1.2,1.8,-1.46957615897682E-16));
#6546=CARTESIAN_POINT('',(-1.2,0.9,-1.46957615897682E-16));
#6547=CARTESIAN_POINT('Origin',(0.,1.8,0.));
#6548=CARTESIAN_POINT('Origin',(1.45,2.8,0.));
#6549=CARTESIAN_POINT('',(-1.45,2.8,-1.77573785876366E-16));
#6550=CARTESIAN_POINT('Origin',(0.,2.8,0.));
#6551=CARTESIAN_POINT('Origin',(0.,2.3,0.));
#6552=CARTESIAN_POINT('',(-1.45,1.8,-1.77573785876366E-16));
#6553=CARTESIAN_POINT('Origin',(0.,1.8,0.));
#6554=CARTESIAN_POINT('',(-1.45,2.3,-1.77573785876366E-16));
#6555=CARTESIAN_POINT('Origin',(1.2,1.8,0.));
#6556=CARTESIAN_POINT('Origin',(1.8,1.45,0.));
#6557=CARTESIAN_POINT('',(1.8,-1.45,-1.77573785876366E-16));
#6558=CARTESIAN_POINT('Origin',(1.8,0.,0.));
#6559=CARTESIAN_POINT('',(1.8,-1.2,-1.46957615897682E-16));
#6560=CARTESIAN_POINT('Origin',(1.8,0.,0.));
#6561=CARTESIAN_POINT('Origin',(2.3,0.,0.));
#6562=CARTESIAN_POINT('',(2.8,-1.45,-1.77573785876366E-16));
#6563=CARTESIAN_POINT('Origin',(2.8,0.,0.));
#6564=CARTESIAN_POINT('',(2.3,-1.45,-1.77573785876366E-16));
#6565=CARTESIAN_POINT('Origin',(2.8,0.,0.));
#6566=CARTESIAN_POINT('Origin',(0.9,0.,0.));
#6567=CARTESIAN_POINT('',(0.9,-1.2,-1.46957615897682E-16));
#6852=UNCERTAINTY_MEASURE_WITH_UNIT(LENGTH_MEASURE(0.001),#6879,
'DISTANCE_ACCURACY_VALUE',
'Maximum model space distance between geometric entities at asserted c
onnectivities');
#6857=UNCERTAINTY_MEASURE_WITH_UNIT(LENGTH_MEASURE(0.001),#6879,
'DISTANCE_ACCURACY_VALUE',
'Maximum model space distance between geometric entities at asserted c
onnectivities');
#6873=(
GEOMETRIC_REPRESENTATION_CONTEXT(3)
GLOBAL_UNCERTAINTY_ASSIGNED_CONTEXT((#6852))
GLOBAL_UNIT_ASSIGNED_CONTEXT((#6879,#6881,#6882))
REPRESENTATION_CONTEXT('','3D')
);
#6878=(
GEOMETRIC_REPRESENTATION_CONTEXT(3)
GLOBAL_UNCERTAINTY_ASSIGNED_CONTEXT((#6857))
GLOBAL_UNIT_ASSIGNED_CONTEXT((#6879,#6881,#6882))
REPRESENTATION_CONTEXT('','3D')
);
#6879=(
LENGTH_UNIT()
NAMED_UNIT(*)
SI_UNIT(.CENTI.,.METRE.)
);
#6881=(
NAMED_UNIT(*)
PLANE_ANGLE_UNIT()
SI_UNIT($,.RADIAN.)
);
#6882=(
NAMED_UNIT(*)
SI_UNIT($,.STERADIAN.)
SOLID_ANGLE_UNIT()
);
#6898=SHAPE_DEFINITION_REPRESENTATION(#6918,#6978);
#6918=PRODUCT_DEFINITION_SHAPE('',$,#6999);
#6978=SHAPE_REPRESENTATION('',(#4379),#6873);
#6983=PRODUCT_DEFINITION_CONTEXT('part definition',#7045,'design');
#6999=PRODUCT_DEFINITION('Pipe Elbow - 90 Degrees, 1-2 Inch Tapered Pipe Thread',
'Pipe Elbow - 90 Degrees, 1-2 Inch Tapered Pipe Thread',#7019,#6983);
#7019=PRODUCT_DEFINITION_FORMATION('',$,#7062);
#7045=APPLICATION_CONTEXT(
'Core Data for Automotive Mechanical Design Process');
#7046=PRODUCT_CONTEXT('part definition',#7045,'mechanical');
#7062=PRODUCT('Pipe Elbow - 90 Degrees, 1-2 Inch Tapered Pipe Thread',
'Pipe Elbow - 90 Degrees, 1-2 Inch Tapered Pipe Thread',
'Pipe Elbow - 90 Degrees, 1-2 Inch Tapered Pipe Thread',(#7046));
#7109=COLOUR_RGB('Light Blue',0.38,0.62,0.78);
#7110=FILL_AREA_STYLE_COLOUR('',#7109);
#7111=FILL_AREA_STYLE('',(#7110));
#7112=SURFACE_STYLE_FILL_AREA(#7111);
#7113=SURFACE_SIDE_STYLE('',(#7112));
#7114=SURFACE_STYLE_USAGE(.BOTH.,#7113);
#7115=PRESENTATION_STYLE_ASSIGNMENT((#7114));
ENDSEC;
END-ISO-10303-21;
